ISO-10303-21;
HEADER;
FILE_DESCRIPTION (('STEP AP214'),
    '1' );
FILE_NAME ('Pivot Pin.step',
    '2026-10-06T08:24:18',
    ( '' ),
    ( '' ),
    'SwSTEP 2.0',
    'SolidWorks 2020',
    '' );
FILE_SCHEMA (( 'AUTOMOTIVE_DESIGN' ));
ENDSEC;

DATA;
#88=EDGE_CURVE ( 'NONE', #8095, #9479, #7286, .T. ) ;
#91=EDGE_LOOP ( 'NONE', ( #1793, #4916 ) ) ;
#195=( NAMED_UNIT ( * ) SI_UNIT ( $, .STERADIAN. ) SOLID_ANGLE_UNIT ( ) );
#209=DIRECTION ( 'NONE',  ( 0.000000000000000000, -1.000000000000000000, 0.000000000000000000 ) ) ;
#254=SURFACE_STYLE_USAGE ( .BOTH. , #2118 ) ;
#281=PRODUCT_DEFINITION_FORMATION_WITH_SPECIFIED_SOURCE ( 'ANY', '', #6035, .NOT_KNOWN. ) ;
#351=PRESENTATION_STYLE_ASSIGNMENT (( #254 ) ) ;
#457=EDGE_CURVE ( 'NONE', #8095, #5909, #7178, .T. ) ;
#500=CARTESIAN_POINT ( 'NONE',  ( -2.000000000000000000, 2.500000000000000000, -414.5000000000000000 ) ) ;
#514=VERTEX_POINT ( 'NONE', #8144 ) ;
#630=EDGE_LOOP ( 'NONE', ( #9121, #1586 ) ) ;
#687=CARTESIAN_POINT ( 'NONE',  ( -2.000000000000000000, -9.500000000000000000, -404.4999999999999432 ) ) ;
#699=DIRECTION ( 'NONE',  ( 0.000000000000000000, -1.000000000000000000, 0.000000000000000000 ) ) ;
#708=SHAPE_DEFINITION_REPRESENTATION ( #7165, #4020 ) ;
#711=DIRECTION ( 'NONE',  ( 0.000000000000000000, -1.000000000000000000, 0.000000000000000000 ) ) ;
#732=VECTOR ( 'NONE', #8909, 1000.000000000000000 ) ;
#774=DIRECTION ( 'NONE',  ( 0.000000000000000000, -1.000000000000000000, 0.000000000000000000 ) ) ;
#837=ORIENTED_EDGE ( 'NONE', *, *, #2330, .F. ) ;
#863=VERTEX_POINT ( 'NONE', #6651 ) ;
#887=CARTESIAN_POINT ( 'NONE',  ( -2.000000000000000000, -9.500000000000000000, -409.5000000000000000 ) ) ;
#888=ADVANCED_FACE ( 'NONE', ( #8362 ), #4180, .T. ) ;
#891=AXIS2_PLACEMENT_3D ( 'NONE', #2634, #7571, #8267 ) ;
#921=AXIS2_PLACEMENT_3D ( 'NONE', #9148, #6732, #8389 ) ;
#969=ORIENTED_EDGE ( 'NONE', *, *, #8738, .F. ) ;
#991=PRESENTATION_STYLE_ASSIGNMENT (( #2911 ) ) ;
#1039=ORIENTED_EDGE ( 'NONE', *, *, #6534, .T. ) ;
#1115=FACE_OUTER_BOUND ( 'NONE', #8891, .T. ) ;
#1176=CARTESIAN_POINT ( 'NONE',  ( -2.000000000000000000, -9.500000000000000000, -414.5000000000000000 ) ) ;
#1182=DIRECTION ( 'NONE',  ( 0.000000000000000000, -1.000000000000000000, 0.000000000000000000 ) ) ;
#1247=ORIENTED_EDGE ( 'NONE', *, *, #6953, .F. ) ;
#1283=MECHANICAL_DESIGN_GEOMETRIC_PRESENTATION_REPRESENTATION('',(#8325),#10048);
#1415=FACE_BOUND ( 'NONE', #6968, .T. ) ;
#1425=CIRCLE ( 'NONE', #9488, 5.000000000000004441 ) ;
#1439=CARTESIAN_POINT ( 'NONE',  ( -2.000000000000000000, 4.200000000000000178, -409.5000000000000000 ) ) ;
#1509=ORIENTED_EDGE ( 'NONE', *, *, #6127, .T. ) ;
#1534=CARTESIAN_POINT ( 'NONE',  ( -2.000000000000000000, -9.500000000000000000, -413.0000000000000000 ) ) ;
#1569=CARTESIAN_POINT ( 'NONE',  ( -2.000000000000000000, 2.500000000000000000, -409.5000000000000000 ) ) ;
#1584=VERTEX_POINT ( 'NONE', #500 ) ;
#1586=ORIENTED_EDGE ( 'NONE', *, *, #7520, .F. ) ;
#1617=ADVANCED_FACE ( 'NONE', ( #2164 ), #2915, .T. ) ;
#1670=DIRECTION ( 'NONE',  ( 0.000000000000000000, 0.000000000000000000, -1.000000000000000000 ) ) ;
#1713=DIRECTION ( 'NONE',  ( 0.000000000000000000, 0.000000000000000000, -1.000000000000000000 ) ) ;
#1719=ORIENTED_EDGE ( 'NONE', *, *, #10081, .T. ) ;
#1723=CIRCLE ( 'NONE', #7116, 3.500000000000003109 ) ;
#1750=ORIENTED_EDGE ( 'NONE', *, *, #3580, .F. ) ;
#1758=DIRECTION ( 'NONE',  ( 0.000000000000000000, -1.000000000000000000, 0.000000000000000000 ) ) ;
#1791=DIRECTION ( 'NONE',  ( 0.000000000000000000, -1.000000000000000000, 0.000000000000000000 ) ) ;
#1793=ORIENTED_EDGE ( 'NONE', *, *, #9309, .F. ) ;
#1809=CARTESIAN_POINT ( 'NONE',  ( -2.000000000000000000, 3.500000000000000000, -404.4999999999999432 ) ) ;
#1810=ORIENTED_EDGE ( 'NONE', *, *, #5332, .T. ) ;
#1828=CARTESIAN_POINT ( 'NONE',  ( -2.000000000000000000, -10.50000000000000000, -414.5000000000000000 ) ) ;
#1926=VECTOR ( 'NONE', #8462, 1000.000000000000000 ) ;
#1951=CYLINDRICAL_SURFACE ( 'NONE', #8230, 5.000000000000004441 ) ;
#2021=ORIENTED_EDGE ( 'NONE', *, *, #4165, .F. ) ;
#2049=CARTESIAN_POINT ( 'NONE',  ( -2.000000000000000000, 3.500000000000000000, -414.5000000000000000 ) ) ;
#2052=( NAMED_UNIT ( * ) PLANE_ANGLE_UNIT ( ) SI_UNIT ( $, .RADIAN. ) );
#2118=SURFACE_SIDE_STYLE ('',( #9331 ) ) ;
#2164=FACE_OUTER_BOUND ( 'NONE', #3632, .T. ) ;
#2243=CARTESIAN_POINT ( 'NONE',  ( -2.000000000000000000, -10.50000000000000000, -409.5000000000000000 ) ) ;
#2249=CARTESIAN_POINT ( 'NONE',  ( -2.000000000000000000, -9.500000000000000000, -404.4999999999999432 ) ) ;
#2330=EDGE_CURVE ( 'NONE', #863, #1584, #7052, .T. ) ;
#2335=FACE_OUTER_BOUND ( 'NONE', #5716, .T. ) ;
#2338=ORIENTED_EDGE ( 'NONE', *, *, #3580, .T. ) ;
#2365=CARTESIAN_POINT ( 'NONE',  ( -2.000000000000000000, 3.500000000000000000, -404.4999999999999432 ) ) ;
#2464=EDGE_CURVE ( 'NONE', #863, #8555, #9746, .T. ) ;
#2634=CARTESIAN_POINT ( 'NONE',  ( -2.000000000000000000, 2.500000000000000000, -409.5000000000000000 ) ) ;
#2668=( NAMED_UNIT ( * ) SI_UNIT ( $, .STERADIAN. ) SOLID_ANGLE_UNIT ( ) );
#2672=CARTESIAN_POINT ( 'NONE',  ( -2.000000000000000000, -9.500000000000000000, -406.0000000000000000 ) ) ;
#2754=DIRECTION ( 'NONE',  ( 0.000000000000000000, 0.000000000000000000, -1.000000000000000000 ) ) ;
#2770=FILL_AREA_STYLE_COLOUR ( '', #5918 ) ;
#2778=ADVANCED_FACE ( 'NONE', ( #10309, #7885 ), #2945, .T. ) ;
#2817=AXIS2_PLACEMENT_3D ( 'NONE', #8634, #3966, #3161 ) ;
#2824=VERTEX_POINT ( 'NONE', #4557 ) ;
#2836=CIRCLE ( 'NONE', #8833, 5.000000000000004441 ) ;
#2849=( GEOMETRIC_REPRESENTATION_CONTEXT ( 3 ) GLOBAL_UNCERTAINTY_ASSIGNED_CONTEXT ( ( #8497 ) ) GLOBAL_UNIT_ASSIGNED_CONTEXT ( ( #4168, #2052, #2668 ) ) REPRESENTATION_CONTEXT ( 'NONE', 'WORKASPACE' ) );
#2908=AXIS2_PLACEMENT_3D ( 'NONE', #8831, #8134, #5760 ) ;
#2911=SURFACE_STYLE_USAGE ( .BOTH. , #5936 ) ;
#2915=CYLINDRICAL_SURFACE ( 'NONE', #8475, 5.000000000000004441 ) ;
#2919=CIRCLE ( 'NONE', #6692, 3.500000000000003109 ) ;
#2945=PLANE ( 'NONE',  #10093 ) ;
#2966=AXIS2_PLACEMENT_3D ( 'NONE', #5653, #774, #6466 ) ;
#2973=CARTESIAN_POINT ( 'NONE',  ( -2.000000000000000000, -10.50000000000000000, -409.5000000000000000 ) ) ;
#3083=ORIENTED_EDGE ( 'NONE', *, *, #9291, .F. ) ;
#3161=DIRECTION ( 'NONE',  ( 1.000000000000000000, 0.000000000000000000, 0.000000000000000000 ) ) ;
#3215=DIRECTION ( 'NONE',  ( -1.000000000000000000, 0.000000000000000000, 0.000000000000000000 ) ) ;
#3274=LINE ( 'NONE', #2365, #5569 ) ;
#3457=FACE_OUTER_BOUND ( 'NONE', #6132, .T. ) ;
#3562=FACE_OUTER_BOUND ( 'NONE', #9580, .T. ) ;
#3580=EDGE_CURVE ( 'NONE', #9479, #514, #10411, .T. ) ;
#3632=EDGE_LOOP ( 'NONE', ( #8374, #2338, #2021, #4086 ) ) ;
#3680=( LENGTH_UNIT ( ) NAMED_UNIT ( * ) SI_UNIT ( .MILLI., .METRE. ) );
#3719=ADVANCED_FACE ( 'NONE', ( #1115 ), #7565, .T. ) ;
#3754=DIRECTION ( 'NONE',  ( -1.000000000000000000, 0.000000000000000000, 0.000000000000000000 ) ) ;
#3911=CARTESIAN_POINT ( 'NONE',  ( -2.000000000000000000, 2.500000000000000000, -409.5000000000000000 ) ) ;
#3935=DIRECTION ( 'NONE',  ( 0.000000000000000000, -1.000000000000000000, 0.000000000000000000 ) ) ;
#3937=ORIENTED_EDGE ( 'NONE', *, *, #5938, .F. ) ;
#3964=DIRECTION ( 'NONE',  ( 0.000000000000000000, -1.000000000000000000, 0.000000000000000000 ) ) ;
#3966=DIRECTION ( 'NONE',  ( 0.000000000000000000, 0.000000000000000000, 1.000000000000000000 ) ) ;
#3983=DIRECTION ( 'NONE',  ( 0.000000000000000000, 0.000000000000000000, -1.000000000000000000 ) ) ;
#4020=SHAPE_REPRESENTATION ( 'Pivot Pin', ( #2817 ), #2849 ) ;
#4079=AXIS2_PLACEMENT_3D ( 'NONE', #5746, #6448, #9620 ) ;
#4086=ORIENTED_EDGE ( 'NONE', *, *, #457, .F. ) ;
#4135=AXIS2_PLACEMENT_3D ( 'NONE', #5568, #3964, #3215 ) ;
#4153=ADVANCED_FACE ( 'NONE', ( #1415, #2335 ), #6356, .F. ) ;
#4165=EDGE_CURVE ( 'NONE', #5909, #514, #1425, .T. ) ;
#4168=( LENGTH_UNIT ( ) NAMED_UNIT ( * ) SI_UNIT ( .MILLI., .METRE. ) );
#4180=CYLINDRICAL_SURFACE ( 'NONE', #7883, 5.000000000000004441 ) ;
#4201=ORIENTED_EDGE ( 'NONE', *, *, #457, .T. ) ;
#4222=( NAMED_UNIT ( * ) PLANE_ANGLE_UNIT ( ) SI_UNIT ( $, .RADIAN. ) );
#4391=ORIENTED_EDGE ( 'NONE', *, *, #6127, .F. ) ;
#4429=ADVANCED_BREP_SHAPE_REPRESENTATION ( '', ( #5374, #2817 ), #2849 ) ;
#4502=DIRECTION ( 'NONE',  ( -1.000000000000000000, 0.000000000000000000, 0.000000000000000000 ) ) ;
#4529=AXIS2_PLACEMENT_3D ( 'NONE', #8639, #4564, #3754 ) ;
#4546=APPLICATION_CONTEXT ( 'automotive_design' ) ;
#4557=CARTESIAN_POINT ( 'NONE',  ( -2.000000000000000000, 2.500000000000000000, -404.4999999999999432 ) ) ;
#4564=DIRECTION ( 'NONE',  ( 0.000000000000000000, -1.000000000000000000, 0.000000000000000000 ) ) ;
#4605=VERTEX_POINT ( 'NONE', #1534 ) ;
#4739=( GEOMETRIC_REPRESENTATION_CONTEXT ( 3 ) GLOBAL_UNCERTAINTY_ASSIGNED_CONTEXT ( ( #4753 ) ) GLOBAL_UNIT_ASSIGNED_CONTEXT ( ( #7848, #4222, #195 ) ) REPRESENTATION_CONTEXT ( 'NONE', 'WORKASPACE' ) );
#4753=UNCERTAINTY_MEASURE_WITH_UNIT (LENGTH_MEASURE( 1.000000000000000082E-05 ), #7848, 'distance_accuracy_value', 'NONE');
#4794=ORIENTED_EDGE ( 'NONE', *, *, #88, .F. ) ;
#4916=ORIENTED_EDGE ( 'NONE', *, *, #2464, .T. ) ;
#4958=PRODUCT_DEFINITION_CONTEXT ( 'detailed design', #8451, 'design' ) ;
#5062=CARTESIAN_POINT ( 'NONE',  ( -2.000000000000000000, 4.200000000000000178, -409.5000000000000000 ) ) ;
#5079=ORIENTED_EDGE ( 'NONE', *, *, #9823, .T. ) ;
#5131=DIRECTION ( 'NONE',  ( 0.000000000000000000, 0.000000000000000000, -1.000000000000000000 ) ) ;
#5156=DIRECTION ( 'NONE',  ( 0.000000000000000000, -1.000000000000000000, 0.000000000000000000 ) ) ;
#5189=CARTESIAN_POINT ( 'NONE',  ( -2.000000000000000000, 2.500000000000000000, -413.0000000000000000 ) ) ;
#5211=VECTOR ( 'NONE', #6365, 1000.000000000000000 ) ;
#5220=CYLINDRICAL_SURFACE ( 'NONE', #8557, 3.500000000000003109 ) ;
#5225=CARTESIAN_POINT ( 'NONE',  ( -2.000000000000000000, 2.500000000000000000, -406.0000000000000000 ) ) ;
#5271=VECTOR ( 'NONE', #1182, 1000.000000000000000 ) ;
#5301=VERTEX_POINT ( 'NONE', #2672 ) ;
#5332=EDGE_CURVE ( 'NONE', #8095, #9479, #2836, .T. ) ;
#5360=PLANE ( 'NONE',  #4529 ) ;
#5374=MANIFOLD_SOLID_BREP ( 'Stock-MAS-686-1', #9511 ) ;
#5415=FACE_OUTER_BOUND ( 'NONE', #6240, .T. ) ;
#5430=DIRECTION ( 'NONE',  ( 0.000000000000000000, 0.000000000000000000, -1.000000000000000000 ) ) ;
#5512=DIRECTION ( 'NONE',  ( 0.000000000000000000, 0.000000000000000000, -1.000000000000000000 ) ) ;
#5513=FACE_OUTER_BOUND ( 'NONE', #91, .T. ) ;
#5516=CYLINDRICAL_SURFACE ( 'NONE', #7273, 3.500000000000003109 ) ;
#5568=CARTESIAN_POINT ( 'NONE',  ( -2.000000000000000000, 3.500000000000000000, -409.5000000000000000 ) ) ;
#5569=VECTOR ( 'NONE', #5738, 1000.000000000000000 ) ;
#5653=CARTESIAN_POINT ( 'NONE',  ( -2.000000000000000000, -9.500000000000000000, -409.5000000000000000 ) ) ;
#5714=ORIENTED_EDGE ( 'NONE', *, *, #6534, .F. ) ;
#5716=EDGE_LOOP ( 'NONE', ( #1810, #4794 ) ) ;
#5721=AXIS2_PLACEMENT_3D ( 'NONE', #2243, #7351, #5512 ) ;
#5738=DIRECTION ( 'NONE',  ( 0.000000000000000000, -1.000000000000000000, 0.000000000000000000 ) ) ;
#5746=CARTESIAN_POINT ( 'NONE',  ( -2.000000000000000000, 3.500000000000000000, -409.5000000000000000 ) ) ;
#5760=DIRECTION ( 'NONE',  ( 0.000000000000000000, 0.000000000000000000, -1.000000000000000000 ) ) ;
#5763=MECHANICAL_DESIGN_GEOMETRIC_PRESENTATION_REPRESENTATION('',(#8171),#4739);
#5774=DIRECTION ( 'NONE',  ( 0.000000000000000000, 1.000000000000000000, 0.000000000000000000 ) ) ;
#5845=ORIENTED_EDGE ( 'NONE', *, *, #7520, .T. ) ;
#5909=VERTEX_POINT ( 'NONE', #1828 ) ;
#5918=COLOUR_RGB ( '', 0.72549020, 0.75294118, 0.79215686) ;
#5936=SURFACE_SIDE_STYLE ('',( #7056 ) ) ;
#5937=COLOUR_RGB ( '', 0.72549020, 0.75294118, 0.79215686) ;
#5938=EDGE_CURVE ( 'NONE', #1584, #2824, #8603, .T. ) ;
#5964=ORIENTED_EDGE ( 'NONE', *, *, #9309, .T. ) ;
#5979=DIRECTION ( 'NONE',  ( 0.000000000000000000, -1.000000000000000000, 0.000000000000000000 ) ) ;
#5988=AXIS2_PLACEMENT_3D ( 'NONE', #3911, #6492, #7404 ) ;
#5993=LINE ( 'NONE', #5189, #1926 ) ;
#6026=DIRECTION ( 'NONE',  ( 0.000000000000000000, 0.000000000000000000, -1.000000000000000000 ) ) ;
#6035=PRODUCT ( 'Pivot Pin', 'Pivot Pin', '', ( #8063 ) ) ;
#6043=ORIENTED_EDGE ( 'NONE', *, *, #9291, .T. ) ;
#6100=ORIENTED_EDGE ( 'NONE', *, *, #6953, .T. ) ;
#6127=EDGE_CURVE ( 'NONE', #8053, #4605, #5993, .T. ) ;
#6132=EDGE_LOOP ( 'NONE', ( #5079, #5714, #1247, #1509 ) ) ;
#6240=EDGE_LOOP ( 'NONE', ( #8071, #6580 ) ) ;
#6293=CARTESIAN_POINT ( 'NONE',  ( -2.000000000000000000, 4.200000000000000178, -409.5000000000000000 ) ) ;
#6356=PLANE ( 'NONE',  #2966 ) ;
#6365=DIRECTION ( 'NONE',  ( 0.000000000000000000, -1.000000000000000000, 0.000000000000000000 ) ) ;
#6434=CIRCLE ( 'NONE', #10211, 5.000000000000004441 ) ;
#6439=CARTESIAN_POINT ( 'NONE',  ( -2.000000000000000000, 2.500000000000000000, -406.0000000000000000 ) ) ;
#6448=DIRECTION ( 'NONE',  ( 0.000000000000000000, 1.000000000000000000, 0.000000000000000000 ) ) ;
#6466=DIRECTION ( 'NONE',  ( -1.000000000000000000, 0.000000000000000000, 0.000000000000000000 ) ) ;
#6492=DIRECTION ( 'NONE',  ( 0.000000000000000000, 1.000000000000000000, 0.000000000000000000 ) ) ;
#6534=EDGE_CURVE ( 'NONE', #8216, #5301, #8657, .T. ) ;
#6580=ORIENTED_EDGE ( 'NONE', *, *, #10081, .F. ) ;
#6651=CARTESIAN_POINT ( 'NONE',  ( -2.000000000000000000, 3.500000000000000000, -414.5000000000000000 ) ) ;
#6692=AXIS2_PLACEMENT_3D ( 'NONE', #9896, #5156, #1670 ) ;
#6708=CARTESIAN_POINT ( 'NONE',  ( -2.000000000000000000, 4.200000000000000178, -409.5000000000000000 ) ) ;
#6732=DIRECTION ( 'NONE',  ( 0.000000000000000000, -1.000000000000000000, 0.000000000000000000 ) ) ;
#6809=DIRECTION ( 'NONE',  ( 0.000000000000000000, 0.000000000000000000, -1.000000000000000000 ) ) ;
#6912=DIRECTION ( 'NONE',  ( 0.000000000000000000, 1.000000000000000000, 0.000000000000000000 ) ) ;
#6953=EDGE_CURVE ( 'NONE', #8053, #8216, #9031, .T. ) ;
#6968=EDGE_LOOP ( 'NONE', ( #8500, #9497 ) ) ;
#7002=FILL_AREA_STYLE_COLOUR ( '', #5937 ) ;
#7034=ORIENTED_EDGE ( 'NONE', *, *, #2464, .F. ) ;
#7052=LINE ( 'NONE', #2049, #5271 ) ;
#7056=SURFACE_STYLE_FILL_AREA ( #8651 ) ;
#7116=AXIS2_PLACEMENT_3D ( 'NONE', #1569, #711, #3983 ) ;
#7140=ADVANCED_FACE ( 'NONE', ( #5513 ), #9659, .F. ) ;
#7142=DIRECTION ( 'NONE',  ( 0.000000000000000000, 0.000000000000000000, -1.000000000000000000 ) ) ;
#7165=PRODUCT_DEFINITION_SHAPE ( 'NONE', 'NONE',  #8684 ) ;
#7166=EDGE_LOOP ( 'NONE', ( #7516, #1039, #9196, #4391 ) ) ;
#7173=ORIENTED_EDGE ( 'NONE', *, *, #5332, .F. ) ;
#7178=LINE ( 'NONE', #8894, #5211 ) ;
#7199=DIRECTION ( 'NONE',  ( 0.000000000000000000, 0.000000000000000000, -1.000000000000000000 ) ) ;
#7273=AXIS2_PLACEMENT_3D ( 'NONE', #1439, #7832, #7142 ) ;
#7286=CIRCLE ( 'NONE', #921, 5.000000000000004441 ) ;
#7301=AXIS2_PLACEMENT_3D ( 'NONE', #9283, #6912, #6809 ) ;
#7351=DIRECTION ( 'NONE',  ( 0.000000000000000000, 1.000000000000000000, 0.000000000000000000 ) ) ;
#7404=DIRECTION ( 'NONE',  ( 0.000000000000000000, 0.000000000000000000, -1.000000000000000000 ) ) ;
#7425=( NAMED_UNIT ( * ) SI_UNIT ( $, .STERADIAN. ) SOLID_ANGLE_UNIT ( ) );
#7453=DIRECTION ( 'NONE',  ( 0.000000000000000000, 0.000000000000000000, -1.000000000000000000 ) ) ;
#7516=ORIENTED_EDGE ( 'NONE', *, *, #8738, .T. ) ;
#7520=EDGE_CURVE ( 'NONE', #1584, #2824, #10449, .T. ) ;
#7565=CYLINDRICAL_SURFACE ( 'NONE', #8444, 5.000000000000004441 ) ;
#7571=DIRECTION ( 'NONE',  ( 0.000000000000000000, -1.000000000000000000, 0.000000000000000000 ) ) ;
#7653=ADVANCED_FACE ( 'NONE', ( #3562 ), #1951, .T. ) ;
#7661=FILL_AREA_STYLE ('',( #2770 ) ) ;
#7722=ADVANCED_FACE ( 'NONE', ( #3457 ), #5220, .T. ) ;
#7832=DIRECTION ( 'NONE',  ( 0.000000000000000000, -1.000000000000000000, 0.000000000000000000 ) ) ;
#7848=( LENGTH_UNIT ( ) NAMED_UNIT ( * ) SI_UNIT ( .MILLI., .METRE. ) );
#7883=AXIS2_PLACEMENT_3D ( 'NONE', #10063, #1758, #7453 ) ;
#7885=FACE_OUTER_BOUND ( 'NONE', #630, .T. ) ;
#7949=EDGE_LOOP ( 'NONE', ( #6100, #969 ) ) ;
#7971=EDGE_CURVE ( 'NONE', #4605, #5301, #2919, .T. ) ;
#8046=FACE_OUTER_BOUND ( 'NONE', #7166, .T. ) ;
#8053=VERTEX_POINT ( 'NONE', #10000 ) ;
#8063=PRODUCT_CONTEXT ( 'NONE', #4546, 'mechanical' ) ;
#8071=ORIENTED_EDGE ( 'NONE', *, *, #4165, .T. ) ;
#8095=VERTEX_POINT ( 'NONE', #1176 ) ;
#8134=DIRECTION ( 'NONE',  ( 0.000000000000000000, 1.000000000000000000, 0.000000000000000000 ) ) ;
#8144=CARTESIAN_POINT ( 'NONE',  ( -2.000000000000000000, -10.50000000000000000, -404.4999999999999432 ) ) ;
#8146=CIRCLE ( 'NONE', #7301, 3.500000000000003109 ) ;
#8171=STYLED_ITEM ( 'NONE', ( #991 ), #4429 ) ;
#8186=UNCERTAINTY_MEASURE_WITH_UNIT (LENGTH_MEASURE( 1.000000000000000082E-05 ), #3680, 'distance_accuracy_value', 'NONE');
#8216=VERTEX_POINT ( 'NONE', #6439 ) ;
#8224=( NAMED_UNIT ( * ) PLANE_ANGLE_UNIT ( ) SI_UNIT ( $, .RADIAN. ) );
#8230=AXIS2_PLACEMENT_3D ( 'NONE', #8499, #1791, #6026 ) ;
#8267=DIRECTION ( 'NONE',  ( 0.000000000000000000, 0.000000000000000000, -1.000000000000000000 ) ) ;
#8325=STYLED_ITEM ( 'NONE', ( #351 ), #5374 ) ;
#8362=FACE_OUTER_BOUND ( 'NONE', #10097, .T. ) ;
#8374=ORIENTED_EDGE ( 'NONE', *, *, #88, .T. ) ;
#8389=DIRECTION ( 'NONE',  ( 0.000000000000000000, 0.000000000000000000, -1.000000000000000000 ) ) ;
#8444=AXIS2_PLACEMENT_3D ( 'NONE', #6708, #209, #1713 ) ;
#8451=APPLICATION_CONTEXT ( 'automotive_design' ) ;
#8462=DIRECTION ( 'NONE',  ( 0.000000000000000000, -1.000000000000000000, 0.000000000000000000 ) ) ;
#8475=AXIS2_PLACEMENT_3D ( 'NONE', #6293, #3935, #5430 ) ;
#8497=UNCERTAINTY_MEASURE_WITH_UNIT (LENGTH_MEASURE( 1.000000000000000082E-05 ), #4168, 'distance_accuracy_value', 'NONE');
#8499=CARTESIAN_POINT ( 'NONE',  ( -2.000000000000000000, 4.200000000000000178, -409.5000000000000000 ) ) ;
#8500=ORIENTED_EDGE ( 'NONE', *, *, #7971, .T. ) ;
#8555=VERTEX_POINT ( 'NONE', #1809 ) ;
#8557=AXIS2_PLACEMENT_3D ( 'NONE', #5062, #9267, #2754 ) ;
#8603=CIRCLE ( 'NONE', #891, 5.000000000000004441 ) ;
#8634=CARTESIAN_POINT ( 'NONE',  ( 0.000000000000000000, 0.000000000000000000, 0.000000000000000000 ) ) ;
#8639=CARTESIAN_POINT ( 'NONE',  ( -2.000000000000000000, -10.50000000000000000, -409.5000000000000000 ) ) ;
#8651=FILL_AREA_STYLE ('',( #7002 ) ) ;
#8657=LINE ( 'NONE', #5225, #9995 ) ;
#8684=PRODUCT_DEFINITION ( 'UNKNOWN', '', #281, #4958 ) ;
#8686=CARTESIAN_POINT ( 'NONE',  ( -2.000000000000000000, 2.500000000000000000, -409.5000000000000000 ) ) ;
#8738=EDGE_CURVE ( 'NONE', #8053, #8216, #1723, .T. ) ;
#8831=CARTESIAN_POINT ( 'NONE',  ( -2.000000000000000000, 2.500000000000000000, -409.5000000000000000 ) ) ;
#8833=AXIS2_PLACEMENT_3D ( 'NONE', #887, #5774, #5131 ) ;
#8891=EDGE_LOOP ( 'NONE', ( #1719, #1750, #7173, #4201 ) ) ;
#8894=CARTESIAN_POINT ( 'NONE',  ( -2.000000000000000000, -9.500000000000000000, -414.5000000000000000 ) ) ;
#8909=DIRECTION ( 'NONE',  ( 0.000000000000000000, -1.000000000000000000, 0.000000000000000000 ) ) ;
#9031=CIRCLE ( 'NONE', #5988, 3.500000000000003109 ) ;
#9113=ADVANCED_FACE ( 'NONE', ( #5415 ), #5360, .T. ) ;
#9121=ORIENTED_EDGE ( 'NONE', *, *, #5938, .T. ) ;
#9148=CARTESIAN_POINT ( 'NONE',  ( -2.000000000000000000, -9.500000000000000000, -409.5000000000000000 ) ) ;
#9196=ORIENTED_EDGE ( 'NONE', *, *, #7971, .F. ) ;
#9267=DIRECTION ( 'NONE',  ( 0.000000000000000000, -1.000000000000000000, 0.000000000000000000 ) ) ;
#9283=CARTESIAN_POINT ( 'NONE',  ( -2.000000000000000000, -9.500000000000000000, -409.5000000000000000 ) ) ;
#9291=EDGE_CURVE ( 'NONE', #8555, #2824, #3274, .T. ) ;
#9309=EDGE_CURVE ( 'NONE', #863, #8555, #6434, .T. ) ;
#9331=SURFACE_STYLE_FILL_AREA ( #7661 ) ;
#9479=VERTEX_POINT ( 'NONE', #687 ) ;
#9488=AXIS2_PLACEMENT_3D ( 'NONE', #2973, #9638, #10552 ) ;
#9497=ORIENTED_EDGE ( 'NONE', *, *, #9823, .F. ) ;
#9503=DIRECTION ( 'NONE',  ( 0.000000000000000000, -1.000000000000000000, 0.000000000000000000 ) ) ;
#9511=CLOSED_SHELL ( 'NONE', ( #9113, #3719, #1617, #4153, #7722, #10524, #2778, #888, #7653, #7140 ) ) ;
#9580=EDGE_LOOP ( 'NONE', ( #5845, #3083, #7034, #10440 ) ) ;
#9620=DIRECTION ( 'NONE',  ( 0.000000000000000000, 0.000000000000000000, -1.000000000000000000 ) ) ;
#9638=DIRECTION ( 'NONE',  ( 0.000000000000000000, -1.000000000000000000, 0.000000000000000000 ) ) ;
#9659=PLANE ( 'NONE',  #4135 ) ;
#9746=CIRCLE ( 'NONE', #4079, 5.000000000000004441 ) ;
#9823=EDGE_CURVE ( 'NONE', #4605, #5301, #8146, .T. ) ;
#9896=CARTESIAN_POINT ( 'NONE',  ( -2.000000000000000000, -9.500000000000000000, -409.5000000000000000 ) ) ;
#9995=VECTOR ( 'NONE', #5979, 1000.000000000000000 ) ;
#10000=CARTESIAN_POINT ( 'NONE',  ( -2.000000000000000000, 2.500000000000000000, -413.0000000000000000 ) ) ;
#10048=( GEOMETRIC_REPRESENTATION_CONTEXT ( 3 ) GLOBAL_UNCERTAINTY_ASSIGNED_CONTEXT ( ( #8186 ) ) GLOBAL_UNIT_ASSIGNED_CONTEXT ( ( #3680, #8224, #7425 ) ) REPRESENTATION_CONTEXT ( 'NONE', 'WORKASPACE' ) );
#10063=CARTESIAN_POINT ( 'NONE',  ( -2.000000000000000000, 4.200000000000000178, -409.5000000000000000 ) ) ;
#10081=EDGE_CURVE ( 'NONE', #5909, #514, #10525, .T. ) ;
#10093=AXIS2_PLACEMENT_3D ( 'NONE', #8686, #9503, #4502 ) ;
#10097=EDGE_LOOP ( 'NONE', ( #5964, #6043, #3937, #837 ) ) ;
#10211=AXIS2_PLACEMENT_3D ( 'NONE', #10469, #699, #7199 ) ;
#10274=SHAPE_REPRESENTATION_RELATIONSHIP ( 'NONE' , 'NONE' ,  #4020, #4429 ) ;
#10309=FACE_BOUND ( 'NONE', #7949, .T. ) ;
#10411=LINE ( 'NONE', #2249, #732 ) ;
#10440=ORIENTED_EDGE ( 'NONE', *, *, #2330, .T. ) ;
#10449=CIRCLE ( 'NONE', #2908, 5.000000000000004441 ) ;
#10469=CARTESIAN_POINT ( 'NONE',  ( -2.000000000000000000, 3.500000000000000000, -409.5000000000000000 ) ) ;
#10524=ADVANCED_FACE ( 'NONE', ( #8046 ), #5516, .T. ) ;
#10525=CIRCLE ( 'NONE', #5721, 5.000000000000004441 ) ;
#10552=DIRECTION ( 'NONE',  ( 0.000000000000000000, 0.000000000000000000, -1.000000000000000000 ) ) ;
ENDSEC;
END-ISO-10303-21;
